ISO-10303-21;
HEADER;
FILE_DESCRIPTION((''),'2;1');
FILE_NAME('Flat_Washer_Small.step','2026-10-09T10:33:02-07:00',(''),(''),'','','');
FILE_SCHEMA (('AUTOMOTIVE_DESIGN { 1 0 10303 214 3 1 1 }'));
ENDSEC;
DATA;
#10=MECHANICAL_DESIGN_GEOMETRIC_PRESENTATION_REPRESENTATION('',(#849),#86330);
#470=TOROIDAL_SURFACE('',#36487,2.9375,0.0625) ;
#471=TOROIDAL_SURFACE('',#36497,2.9375,0.0625) ;
#825=SHAPE_REPRESENTATION_RELATIONSHIP('SRR','None',#86475,#837) ;
#837=ADVANCED_BREP_SHAPE_REPRESENTATION('',(#861),#86329) ;
#849=STYLED_ITEM('',(#86582),#861) ;
#861=MANIFOLD_SOLID_BREP('Body1',#32648) ;
#1187=FACE_BOUND('',#6230,.T.) ;
#1188=FACE_BOUND('',#6233,.T.) ;
#2268=PLANE('',#36495) ;
#2269=PLANE('',#36500) ;
#4152=FACE_OUTER_BOUND('',#6227,.T.) ;
#4153=FACE_OUTER_BOUND('',#6228,.T.) ;
#4154=FACE_OUTER_BOUND('',#6229,.T.) ;
#4155=FACE_OUTER_BOUND('',#6231,.T.) ;
#4156=FACE_OUTER_BOUND('',#6232,.T.) ;
#4157=FACE_OUTER_BOUND('',#6234,.T.) ;
#6227=EDGE_LOOP('',(#29924,#29925,#29926,#29927,#29928)) ;
#6228=EDGE_LOOP('',(#29929,#29930,#29931,#29932,#29933,#29934)) ;
#6229=EDGE_LOOP('',(#29935)) ;
#6230=EDGE_LOOP('',(#29936)) ;
#6231=EDGE_LOOP('',(#29937,#29938,#29939,#29940,#29941)) ;
#6232=EDGE_LOOP('',(#29942)) ;
#6233=EDGE_LOOP('',(#29943)) ;
#6234=EDGE_LOOP('',(#29944,#29945,#29946,#29947)) ;
#8552=LINE('',#86246,#10871) ;
#8553=LINE('',#86258,#10872) ;
#10871=VECTOR('',#46288,3.) ;
#10872=VECTOR('',#46305,1.6) ;
#12657=CIRCLE('',#36488,2.9375) ;
#12658=CIRCLE('',#36489,0.0625) ;
#12659=CIRCLE('',#36490,3.) ;
#12660=CIRCLE('',#36491,3.) ;
#12661=CIRCLE('',#36493,3.) ;
#12662=CIRCLE('',#36494,3.) ;
#12663=CIRCLE('',#36496,1.6) ;
#12664=CIRCLE('',#36498,0.0625) ;
#12665=CIRCLE('',#36499,2.9375) ;
#12666=CIRCLE('',#36501,1.6) ;
#15588=VERTEX_POINT('',#86234) ;
#15589=VERTEX_POINT('',#86236) ;
#15590=VERTEX_POINT('',#86238) ;
#15591=VERTEX_POINT('',#86242) ;
#15592=VERTEX_POINT('',#86243) ;
#15593=VERTEX_POINT('',#86248) ;
#15594=VERTEX_POINT('',#86251) ;
#15595=VERTEX_POINT('',#86255) ;
#20368=EDGE_CURVE('',#15588,#15588,#12657,.T.) ;
#20369=EDGE_CURVE('',#15588,#15589,#12658,.T.) ;
#20370=EDGE_CURVE('',#15589,#15590,#12659,.T.) ;
#20371=EDGE_CURVE('',#15590,#15589,#12660,.T.) ;
#20372=EDGE_CURVE('',#15591,#15592,#12661,.T.) ;
#20373=EDGE_CURVE('',#15592,#15591,#12662,.T.) ;
#20374=EDGE_CURVE('',#15592,#15590,#8552,.T.) ;
#20375=EDGE_CURVE('',#15593,#15593,#12663,.T.) ;
#20376=EDGE_CURVE('',#15591,#15594,#12664,.T.) ;
#20377=EDGE_CURVE('',#15594,#15594,#12665,.T.) ;
#20378=EDGE_CURVE('',#15595,#15595,#12666,.T.) ;
#20379=EDGE_CURVE('',#15593,#15595,#8553,.T.) ;
#29924=ORIENTED_EDGE('',*,*,#20368,.T.) ;
#29925=ORIENTED_EDGE('',*,*,#20369,.T.) ;
#29926=ORIENTED_EDGE('',*,*,#20370,.T.) ;
#29927=ORIENTED_EDGE('',*,*,#20371,.T.) ;
#29928=ORIENTED_EDGE('',*,*,#20369,.F.) ;
#29929=ORIENTED_EDGE('',*,*,#20372,.F.) ;
#29930=ORIENTED_EDGE('',*,*,#20373,.F.) ;
#29931=ORIENTED_EDGE('',*,*,#20374,.T.) ;
#29932=ORIENTED_EDGE('',*,*,#20370,.F.) ;
#29933=ORIENTED_EDGE('',*,*,#20371,.F.) ;
#29934=ORIENTED_EDGE('',*,*,#20374,.F.) ;
#29935=ORIENTED_EDGE('',*,*,#20368,.F.) ;
#29936=ORIENTED_EDGE('',*,*,#20375,.F.) ;
#29937=ORIENTED_EDGE('',*,*,#20372,.T.) ;
#29938=ORIENTED_EDGE('',*,*,#20373,.T.) ;
#29939=ORIENTED_EDGE('',*,*,#20376,.T.) ;
#29940=ORIENTED_EDGE('',*,*,#20377,.T.) ;
#29941=ORIENTED_EDGE('',*,*,#20376,.F.) ;
#29942=ORIENTED_EDGE('',*,*,#20377,.F.) ;
#29943=ORIENTED_EDGE('',*,*,#20378,.T.) ;
#29944=ORIENTED_EDGE('',*,*,#20375,.T.) ;
#29945=ORIENTED_EDGE('',*,*,#20379,.T.) ;
#29946=ORIENTED_EDGE('',*,*,#20378,.F.) ;
#29947=ORIENTED_EDGE('',*,*,#20379,.F.) ;
#30747=CYLINDRICAL_SURFACE('',#36492,3.) ;
#30748=CYLINDRICAL_SURFACE('',#36502,1.6) ;
#32631=ADVANCED_FACE('',(#4152),#470,.T.) ;
#32632=ADVANCED_FACE('',(#4153),#30747,.T.) ;
#32633=ADVANCED_FACE('',(#4154,#1187),#2268,.T.) ;
#32634=ADVANCED_FACE('',(#4155),#471,.T.) ;
#32635=ADVANCED_FACE('',(#4156,#1188),#2269,.F.) ;
#32636=ADVANCED_FACE('',(#4157),#30748,.F.) ;
#32648=CLOSED_SHELL('',(#32631,#32632,#32633,#32634,#32635,#32636)) ;
#36486=AXIS2_PLACEMENT_3D('',#86232,#46270,#46271) ;
#36487=AXIS2_PLACEMENT_3D('',#86233,#46272,#46273) ;
#36488=AXIS2_PLACEMENT_3D('',#86235,#46274,#46275) ;
#36489=AXIS2_PLACEMENT_3D('',#86237,#46276,#46277) ;
#36490=AXIS2_PLACEMENT_3D('',#86239,#46278,#46279) ;
#36491=AXIS2_PLACEMENT_3D('',#86240,#46280,#46281) ;
#36492=AXIS2_PLACEMENT_3D('',#86241,#46282,#46283) ;
#36493=AXIS2_PLACEMENT_3D('',#86244,#46284,#46285) ;
#36494=AXIS2_PLACEMENT_3D('',#86245,#46286,#46287) ;
#36495=AXIS2_PLACEMENT_3D('',#86247,#46289,#46290) ;
#36496=AXIS2_PLACEMENT_3D('',#86249,#46291,#46292) ;
#36497=AXIS2_PLACEMENT_3D('',#86250,#46293,#46294) ;
#36498=AXIS2_PLACEMENT_3D('',#86252,#46295,#46296) ;
#36499=AXIS2_PLACEMENT_3D('',#86253,#46297,#46298) ;
#36500=AXIS2_PLACEMENT_3D('',#86254,#46299,#46300) ;
#36501=AXIS2_PLACEMENT_3D('',#86256,#46301,#46302) ;
#36502=AXIS2_PLACEMENT_3D('',#86257,#46303,#46304) ;
#46270=DIRECTION('axis',(0.,0.,1.)) ;
#46271=DIRECTION('refdir',(1.,0.,0.)) ;
#46272=DIRECTION('center_axis',(0.,0.,1.)) ;
#46273=DIRECTION('ref_axis',(1.,0.,0.)) ;
#46274=DIRECTION('center_axis',(0.,0.,-1.)) ;
#46275=DIRECTION('ref_axis',(1.,0.,0.)) ;
#46276=DIRECTION('center_axis',(1.22464679914735E-16,-1.,0.)) ;
#46277=DIRECTION('ref_axis',(-1.,-1.22464679914735E-16,0.)) ;
#46278=DIRECTION('center_axis',(0.,0.,1.)) ;
#46279=DIRECTION('ref_axis',(1.,0.,0.)) ;
#46280=DIRECTION('center_axis',(0.,0.,1.)) ;
#46281=DIRECTION('ref_axis',(1.,0.,0.)) ;
#46282=DIRECTION('center_axis',(0.,0.,-1.)) ;
#46283=DIRECTION('ref_axis',(-1.,0.,0.)) ;
#46284=DIRECTION('center_axis',(0.,0.,-1.)) ;
#46285=DIRECTION('ref_axis',(1.,0.,0.)) ;
#46286=DIRECTION('center_axis',(0.,0.,-1.)) ;
#46287=DIRECTION('ref_axis',(1.,0.,0.)) ;
#46288=DIRECTION('',(0.,0.,1.)) ;
#46289=DIRECTION('center_axis',(0.,0.,1.)) ;
#46290=DIRECTION('ref_axis',(1.,0.,0.)) ;
#46291=DIRECTION('center_axis',(0.,0.,1.)) ;
#46292=DIRECTION('ref_axis',(1.,0.,0.)) ;
#46293=DIRECTION('center_axis',(0.,0.,1.)) ;
#46294=DIRECTION('ref_axis',(1.,0.,0.)) ;
#46295=DIRECTION('center_axis',(1.22464679914735E-16,-1.,0.)) ;
#46296=DIRECTION('ref_axis',(-1.,-1.22464679914735E-16,0.)) ;
#46297=DIRECTION('center_axis',(0.,0.,1.)) ;
#46298=DIRECTION('ref_axis',(1.,0.,0.)) ;
#46299=DIRECTION('center_axis',(0.,0.,1.)) ;
#46300=DIRECTION('ref_axis',(1.,0.,0.)) ;
#46301=DIRECTION('center_axis',(0.,0.,1.)) ;
#46302=DIRECTION('ref_axis',(1.,0.,0.)) ;
#46303=DIRECTION('center_axis',(0.,0.,-1.)) ;
#46304=DIRECTION('ref_axis',(-1.,0.,0.)) ;
#46305=DIRECTION('',(0.,0.,-1.)) ;
#86232=CARTESIAN_POINT('',(0.,0.,0.)) ;
#86233=CARTESIAN_POINT('Origin',(0.,0.,0.2375)) ;
#86234=CARTESIAN_POINT('',(-2.9375,3.59739997249535E-16,0.299999999999999)) ;
#86235=CARTESIAN_POINT('Origin',(0.,0.,0.299999999999999)) ;
#86236=CARTESIAN_POINT('',(-3.,-3.67394039744206E-16,0.2375)) ;
#86237=CARTESIAN_POINT('Origin',(-2.9375,-3.59739997249535E-16,0.2375)) ;
#86238=CARTESIAN_POINT('',(3.,-3.67394039744206E-16,0.2375)) ;
#86239=CARTESIAN_POINT('Origin',(0.,0.,0.2375)) ;
#86240=CARTESIAN_POINT('Origin',(0.,0.,0.2375)) ;
#86241=CARTESIAN_POINT('Origin',(0.,0.,0.299999999999999)) ;
#86242=CARTESIAN_POINT('',(-3.,3.67394039744206E-16,-0.237500000000001)) ;
#86243=CARTESIAN_POINT('',(3.,-3.67394039744206E-16,-0.237500000000001)) ;
#86244=CARTESIAN_POINT('Origin',(0.,0.,-0.237500000000001)) ;
#86245=CARTESIAN_POINT('Origin',(0.,0.,-0.237500000000001)) ;
#86246=CARTESIAN_POINT('',(3.,-3.67394039744206E-16,0.299999999999999)) ;
#86247=CARTESIAN_POINT('Origin',(0.,0.,0.299999999999999)) ;
#86248=CARTESIAN_POINT('',(1.6,-1.95943487863577E-16,0.299999999999999)) ;
#86249=CARTESIAN_POINT('Origin',(0.,0.,0.299999999999999)) ;
#86250=CARTESIAN_POINT('Origin',(0.,0.,-0.237500000000001)) ;
#86251=CARTESIAN_POINT('',(-2.9375,-3.59739997249535E-16,-0.300000000000001)) ;
#86252=CARTESIAN_POINT('Origin',(-2.9375,-3.59739997249535E-16,-0.237500000000001)) ;
#86253=CARTESIAN_POINT('Origin',(0.,0.,-0.300000000000001)) ;
#86254=CARTESIAN_POINT('Origin',(0.,0.,-0.300000000000001)) ;
#86255=CARTESIAN_POINT('',(1.6,-1.95943487863577E-16,-0.300000000000001)) ;
#86256=CARTESIAN_POINT('Origin',(0.,0.,-0.300000000000001)) ;
#86257=CARTESIAN_POINT('Origin',(0.,0.,0.299999999999999)) ;
#86258=CARTESIAN_POINT('',(1.6,-1.95943487863577E-16,0.299999999999999)) ;
#86303=UNCERTAINTY_MEASURE_WITH_UNIT(LENGTH_MEASURE(0.01),#86331,
'DISTANCE_ACCURACY_VALUE',
'Maximum model space distance between geometric entities at asserted c
onnectivities') ;
#86304=UNCERTAINTY_MEASURE_WITH_UNIT(LENGTH_MEASURE(0.01),#86331,
'DISTANCE_ACCURACY_VALUE',
'Maximum model space distance between geometric entities at asserted c
onnectivities') ;
#86329=(
GEOMETRIC_REPRESENTATION_CONTEXT(3)
GLOBAL_UNCERTAINTY_ASSIGNED_CONTEXT((#86303))
GLOBAL_UNIT_ASSIGNED_CONTEXT((#86331,#86333,#86334))
REPRESENTATION_CONTEXT('','3D')
) ;
#86330=(
GEOMETRIC_REPRESENTATION_CONTEXT(3)
GLOBAL_UNCERTAINTY_ASSIGNED_CONTEXT((#86304))
GLOBAL_UNIT_ASSIGNED_CONTEXT((#86331,#86333,#86334))
REPRESENTATION_CONTEXT('','3D')
) ;
#86331=(
LENGTH_UNIT()
NAMED_UNIT(*)
SI_UNIT(.MILLI.,.METRE.)
) ;
#86333=(
NAMED_UNIT(*)
PLANE_ANGLE_UNIT()
SI_UNIT($,.RADIAN.)
) ;
#86334=(
NAMED_UNIT(*)
SI_UNIT($,.STERADIAN.)
SOLID_ANGLE_UNIT()
) ;
#86359=SHAPE_DEFINITION_REPRESENTATION(#86430,#86475) ;
#86430=PRODUCT_DEFINITION_SHAPE('',$,#86501) ;
#86475=SHAPE_REPRESENTATION('',(#36486),#86329) ;
#86476=PRODUCT_DEFINITION_CONTEXT('part definition',#86553,'design') ;
#86501=PRODUCT_DEFINITION('Flat_Washer_Small','Flat_Washer_Small',#86526,
#86476) ;
#86526=PRODUCT_DEFINITION_FORMATION('',$,#86579) ;
#86553=APPLICATION_CONTEXT(
'Core Data for Automotive Mechanical Design Process') ;
#86554=PRODUCT_CONTEXT('part definition',#86553,'mechanical') ;
#86579=PRODUCT('Flat_Washer_Small','Flat_Washer_Small',$,(#86554)) ;
#86582=PRESENTATION_STYLE_ASSIGNMENT((#86587)) ;
#86587=SURFACE_STYLE_USAGE(.BOTH.,#86592) ;
#86592=SURFACE_SIDE_STYLE('',(#86597)) ;
#86597=SURFACE_STYLE_FILL_AREA(#86602) ;
#86602=FILL_AREA_STYLE('Opaque(203,203,203)',(#86607)) ;
#86607=FILL_AREA_STYLE_COLOUR('Opaque(203,203,203)',#86612) ;
#86612=COLOUR_RGB('Opaque(203,203,203)', 0.66274510, 0.83137255, 0.94901961) ;
ENDSEC;
END-ISO-10303-21;
